ISO-10303-21;
HEADER;
/* Generated by software containing ST-Developer
 * from STEP Tools, Inc. (www.steptools.com) 
 */

FILE_DESCRIPTION(
/* description */ ('Air blow-off nozzle station'),
/* implementation_level */ '2;1');

FILE_NAME(
/* name */ 'Flat Washer - M5.step',
/* time_stamp */ '2026-10-27T10:53:54-07:00',
/* author */ (''),
/* organization */ (''),
/* preprocessor_version */ 'ST-DEVELOPER v20.2',
/* originating_system */ 'Autodesk Translation Framework v15.17.0.0',
/* authorisation */ '');

FILE_SCHEMA (('AUTOMOTIVE_DESIGN { 1 0 10303 214 3 1 1 }'));
ENDSEC;

DATA;
#10=MECHANICAL_DESIGN_GEOMETRIC_PRESENTATION_REPRESENTATION('',(#247),#7897);
#155=CONICAL_SURFACE('',#4800,0.275,0.785398163397449);
#197=SHAPE_REPRESENTATION_RELATIONSHIP('SRR','None',#8011,#222);
#222=ADVANCED_BREP_SHAPE_REPRESENTATION('',(#272),#7878);
#247=STYLED_ITEM('',(#8227),#272);
#272=MANIFOLD_SOLID_BREP('Body1',#4296);
#327=FACE_BOUND('',#973,.T.);
#328=FACE_BOUND('',#976,.T.);
#470=PLANE('',#4805);
#471=PLANE('',#4809);
#672=FACE_OUTER_BOUND('',#970,.T.);
#673=FACE_OUTER_BOUND('',#971,.T.);
#674=FACE_OUTER_BOUND('',#972,.T.);
#675=FACE_OUTER_BOUND('',#974,.T.);
#676=FACE_OUTER_BOUND('',#975,.T.);
#970=EDGE_LOOP('',(#3523,#3524,#3525,#3526));
#971=EDGE_LOOP('',(#3527,#3528,#3529,#3530));
#972=EDGE_LOOP('',(#3531));
#973=EDGE_LOOP('',(#3532));
#974=EDGE_LOOP('',(#3533,#3534,#3535,#3536));
#975=EDGE_LOOP('',(#3537));
#976=EDGE_LOOP('',(#3538));
#1369=LINE('',#7297,#1723);
#1370=LINE('',#7301,#1724);
#1371=LINE('',#7308,#1725);
#1723=VECTOR('',#5729,0.275);
#1724=VECTOR('',#5734,0.265);
#1725=VECTOR('',#5743,0.5);
#1912=CIRCLE('',#4801,0.285);
#1913=CIRCLE('',#4802,0.265);
#1914=CIRCLE('',#4804,0.265);
#1915=CIRCLE('',#4806,0.5);
#1916=CIRCLE('',#4808,0.5);
#2220=VERTEX_POINT('',#7294);
#2221=VERTEX_POINT('',#7296);
#2222=VERTEX_POINT('',#7300);
#2223=VERTEX_POINT('',#7304);
#2224=VERTEX_POINT('',#7307);
#2679=EDGE_CURVE('',#2220,#2220,#1912,.T.);
#2680=EDGE_CURVE('',#2220,#2221,#1369,.T.);
#2681=EDGE_CURVE('',#2221,#2221,#1913,.T.);
#2682=EDGE_CURVE('',#2221,#2222,#1370,.T.);
#2683=EDGE_CURVE('',#2222,#2222,#1914,.T.);
#2684=EDGE_CURVE('',#2223,#2223,#1915,.T.);
#2685=EDGE_CURVE('',#2223,#2224,#1371,.T.);
#2686=EDGE_CURVE('',#2224,#2224,#1916,.T.);
#3523=ORIENTED_EDGE('',*,*,#2679,.T.);
#3524=ORIENTED_EDGE('',*,*,#2680,.T.);
#3525=ORIENTED_EDGE('',*,*,#2681,.T.);
#3526=ORIENTED_EDGE('',*,*,#2680,.F.);
#3527=ORIENTED_EDGE('',*,*,#2681,.F.);
#3528=ORIENTED_EDGE('',*,*,#2682,.T.);
#3529=ORIENTED_EDGE('',*,*,#2683,.T.);
#3530=ORIENTED_EDGE('',*,*,#2682,.F.);
#3531=ORIENTED_EDGE('',*,*,#2684,.T.);
#3532=ORIENTED_EDGE('',*,*,#2679,.F.);
#3533=ORIENTED_EDGE('',*,*,#2684,.F.);
#3534=ORIENTED_EDGE('',*,*,#2685,.T.);
#3535=ORIENTED_EDGE('',*,*,#2686,.T.);
#3536=ORIENTED_EDGE('',*,*,#2685,.F.);
#3537=ORIENTED_EDGE('',*,*,#2686,.F.);
#3538=ORIENTED_EDGE('',*,*,#2683,.F.);
#3989=CYLINDRICAL_SURFACE('',#4803,0.265);
#3990=CYLINDRICAL_SURFACE('',#4807,0.5);
#4162=ADVANCED_FACE('',(#672),#155,.F.);
#4163=ADVANCED_FACE('',(#673),#3989,.F.);
#4164=ADVANCED_FACE('',(#674,#327),#470,.T.);
#4165=ADVANCED_FACE('',(#675),#3990,.T.);
#4166=ADVANCED_FACE('',(#676,#328),#471,.F.);
#4296=CLOSED_SHELL('',(#4162,#4163,#4164,#4165,#4166));
#4799=AXIS2_PLACEMENT_3D('',#7292,#5723,#5724);
#4800=AXIS2_PLACEMENT_3D('',#7293,#5725,#5726);
#4801=AXIS2_PLACEMENT_3D('',#7295,#5727,#5728);
#4802=AXIS2_PLACEMENT_3D('',#7298,#5730,#5731);
#4803=AXIS2_PLACEMENT_3D('',#7299,#5732,#5733);
#4804=AXIS2_PLACEMENT_3D('',#7302,#5735,#5736);
#4805=AXIS2_PLACEMENT_3D('',#7303,#5737,#5738);
#4806=AXIS2_PLACEMENT_3D('',#7305,#5739,#5740);
#4807=AXIS2_PLACEMENT_3D('',#7306,#5741,#5742);
#4808=AXIS2_PLACEMENT_3D('',#7309,#5744,#5745);
#4809=AXIS2_PLACEMENT_3D('',#7310,#5746,#5747);
#5723=DIRECTION('axis',(0.,0.,1.));
#5724=DIRECTION('refdir',(1.,0.,0.));
#5725=DIRECTION('center_axis',(0.,1.,0.));
#5726=DIRECTION('ref_axis',(1.,0.,0.));
#5727=DIRECTION('center_axis',(0.,1.,0.));
#5728=DIRECTION('ref_axis',(1.,0.,0.));
#5729=DIRECTION('',(0.707106781186548,-0.707106781186547,-8.65956056235494E-17));
#5730=DIRECTION('center_axis',(0.,-1.,0.));
#5731=DIRECTION('ref_axis',(1.,0.,0.));
#5732=DIRECTION('center_axis',(0.,1.,0.));
#5733=DIRECTION('ref_axis',(1.,0.,0.));
#5734=DIRECTION('',(0.,-1.,0.));
#5735=DIRECTION('center_axis',(0.,-1.,0.));
#5736=DIRECTION('ref_axis',(1.,0.,0.));
#5737=DIRECTION('center_axis',(0.,1.,0.));
#5738=DIRECTION('ref_axis',(1.,0.,0.));
#5739=DIRECTION('center_axis',(0.,1.,0.));
#5740=DIRECTION('ref_axis',(1.,0.,0.));
#5741=DIRECTION('center_axis',(0.,1.,0.));
#5742=DIRECTION('ref_axis',(1.,0.,0.));
#5743=DIRECTION('',(0.,-1.,0.));
#5744=DIRECTION('center_axis',(0.,1.,0.));
#5745=DIRECTION('ref_axis',(1.,0.,0.));
#5746=DIRECTION('center_axis',(0.,1.,0.));
#5747=DIRECTION('ref_axis',(1.,0.,0.));
#7292=CARTESIAN_POINT('',(0.,0.,0.));
#7293=CARTESIAN_POINT('Origin',(0.,0.09,0.));
#7294=CARTESIAN_POINT('',(-0.285,0.1,3.49024337756996E-17));
#7295=CARTESIAN_POINT('Origin',(0.,0.1,0.));
#7296=CARTESIAN_POINT('',(-0.265,0.08,-3.24531401774049E-17));
#7297=CARTESIAN_POINT('',(-0.275,0.09,3.36777869765522E-17));
#7298=CARTESIAN_POINT('Origin',(0.,0.08,0.));
#7299=CARTESIAN_POINT('Origin',(0.,0.,0.));
#7300=CARTESIAN_POINT('',(-0.265,0.,3.24531401774049E-17));
#7301=CARTESIAN_POINT('',(-0.265,0.,3.24531401774049E-17));
#7302=CARTESIAN_POINT('Origin',(0.,0.,0.));
#7303=CARTESIAN_POINT('Origin',(0.,0.1,0.));
#7304=CARTESIAN_POINT('',(-0.5,0.1,6.12323399573677E-17));
#7305=CARTESIAN_POINT('Origin',(0.,0.1,0.));
#7306=CARTESIAN_POINT('Origin',(0.,0.,0.));
#7307=CARTESIAN_POINT('',(-0.5,0.,6.12323399573677E-17));
#7308=CARTESIAN_POINT('',(-0.5,0.,6.12323399573677E-17));
#7309=CARTESIAN_POINT('Origin',(0.,0.,0.));
#7310=CARTESIAN_POINT('Origin',(0.,0.,0.));
#7846=UNCERTAINTY_MEASURE_WITH_UNIT(LENGTH_MEASURE(0.001),#7898,
'DISTANCE_ACCURACY_VALUE',
'Maximum model space distance between geometric entities at asserted c
onnectivities');
#7865=UNCERTAINTY_MEASURE_WITH_UNIT(LENGTH_MEASURE(0.001),#7898,
'DISTANCE_ACCURACY_VALUE',
'Maximum model space distance between geometric entities at asserted c
onnectivities');
#7878=(
GEOMETRIC_REPRESENTATION_CONTEXT(3)
GLOBAL_UNCERTAINTY_ASSIGNED_CONTEXT((#7846))
GLOBAL_UNIT_ASSIGNED_CONTEXT((#7898,#7900,#7901))
REPRESENTATION_CONTEXT('','3D')
);
#7897=(
GEOMETRIC_REPRESENTATION_CONTEXT(3)
GLOBAL_UNCERTAINTY_ASSIGNED_CONTEXT((#7865))
GLOBAL_UNIT_ASSIGNED_CONTEXT((#7898,#7900,#7901))
REPRESENTATION_CONTEXT('','3D')
);
#7898=(
LENGTH_UNIT()
NAMED_UNIT(*)
SI_UNIT(.CENTI.,.METRE.)
);
#7900=(
NAMED_UNIT(*)
PLANE_ANGLE_UNIT()
SI_UNIT($,.RADIAN.)
);
#7901=(
NAMED_UNIT(*)
SI_UNIT($,.STERADIAN.)
SOLID_ANGLE_UNIT()
);
#7914=SHAPE_DEFINITION_REPRESENTATION(#7945,#8011);
#7945=PRODUCT_DEFINITION_SHAPE('',$,#8043);
#8011=SHAPE_REPRESENTATION('',(#4799),#7878);
#8030=PRODUCT_DEFINITION_CONTEXT('part definition',#8125,'design');
#8043=PRODUCT_DEFINITION('Flat Washer - M5','Flat Washer - M5',#8074,#8030);
#8074=PRODUCT_DEFINITION_FORMATION('',$,#8139);
#8125=APPLICATION_CONTEXT(
'Core Data for Automotive Mechanical Design Process');
#8126=PRODUCT_CONTEXT('part definition',#8125,'mechanical');
#8139=PRODUCT('Flat Washer - M5','Flat Washer - M5','Flat Washer - M5',
(#8126));
#8221=COLOUR_RGB('Black',0.12,0.14,0.17);
#8222=FILL_AREA_STYLE_COLOUR('',#8221);
#8223=FILL_AREA_STYLE('',(#8222));
#8224=SURFACE_STYLE_FILL_AREA(#8223);
#8225=SURFACE_SIDE_STYLE('',(#8224));
#8226=SURFACE_STYLE_USAGE(.BOTH.,#8225);
#8227=PRESENTATION_STYLE_ASSIGNMENT((#8226));
ENDSEC;
END-ISO-10303-21;
